ISO-10303-21;
HEADER;
/* Generated by software containing ST-Developer
 * from STEP Tools, Inc. (www.steptools.com) 
 */

FILE_DESCRIPTION(
/* description */ (''),
/* implementation_level */ '2;1');

FILE_NAME(
/* name */ 'End_Block.step',
/* time_stamp */ '2026-10-23T22:29:29+06:00',
/* author */ (''),
/* organization */ (''),
/* preprocessor_version */ 'ST-DEVELOPER v20.2',
/* originating_system */ 'Autodesk Translation Framework v15.15.0.0',
/* authorisation */ '');

FILE_SCHEMA (('AUTOMOTIVE_DESIGN { 1 0 10303 214 3 1 1 }'));
ENDSEC;

DATA;
#10=MECHANICAL_DESIGN_GEOMETRIC_PRESENTATION_REPRESENTATION('',(#78),#7047);
#58=SHAPE_REPRESENTATION_RELATIONSHIP('SRR','None',#7091,#68);
#68=ADVANCED_BREP_SHAPE_REPRESENTATION('',(#91),#7043);
#78=STYLED_ITEM('',(#7177),#91);
#91=MANIFOLD_SOLID_BREP('End_Block',#3403);
#117=FACE_BOUND('',#606,.T.);
#118=FACE_BOUND('',#607,.T.);
#119=FACE_BOUND('',#610,.T.);
#120=FACE_BOUND('',#611,.T.);
#219=PLANE('',#3811);
#220=PLANE('',#3812);
#221=PLANE('',#3813);
#222=PLANE('',#3814);
#223=PLANE('',#3815);
#224=PLANE('',#3816);
#225=PLANE('',#3819);
#226=PLANE('',#3820);
#227=PLANE('',#3823);
#228=PLANE('',#3826);
#401=FACE_OUTER_BOUND('',#600,.T.);
#402=FACE_OUTER_BOUND('',#601,.T.);
#403=FACE_OUTER_BOUND('',#602,.T.);
#404=FACE_OUTER_BOUND('',#603,.T.);
#405=FACE_OUTER_BOUND('',#604,.T.);
#406=FACE_OUTER_BOUND('',#605,.T.);
#407=FACE_OUTER_BOUND('',#608,.T.);
#408=FACE_OUTER_BOUND('',#609,.T.);
#409=FACE_OUTER_BOUND('',#612,.T.);
#410=FACE_OUTER_BOUND('',#613,.T.);
#411=FACE_OUTER_BOUND('',#614,.T.);
#412=FACE_OUTER_BOUND('',#615,.T.);
#600=EDGE_LOOP('',(#2909,#2910,#2911,#2912));
#601=EDGE_LOOP('',(#2913,#2914,#2915,#2916));
#602=EDGE_LOOP('',(#2917,#2918,#2919,#2920));
#603=EDGE_LOOP('',(#2921,#2922,#2923,#2924));
#604=EDGE_LOOP('',(#2925,#2926,#2927,#2928,#2929,#2930,#2931,#2932));
#605=EDGE_LOOP('',(#2933,#2934,#2935,#2936));
#606=EDGE_LOOP('',(#2937));
#607=EDGE_LOOP('',(#2938));
#608=EDGE_LOOP('',(#2939,#2940,#2941,#2942));
#609=EDGE_LOOP('',(#2943,#2944,#2945,#2946,#2947,#2948,#2949,#2950));
#610=EDGE_LOOP('',(#2951));
#611=EDGE_LOOP('',(#2952));
#612=EDGE_LOOP('',(#2953,#2954,#2955,#2956));
#613=EDGE_LOOP('',(#2957,#2958,#2959,#2960));
#614=EDGE_LOOP('',(#2961,#2962,#2963,#2964));
#615=EDGE_LOOP('',(#2965,#2966,#2967,#2968));
#780=CIRCLE('',#3817,2.5175);
#781=CIRCLE('',#3818,2.5175);
#782=CIRCLE('',#3821,2.5175);
#783=CIRCLE('',#3822,2.5175);
#1005=LINE('',#5873,#1299);
#1006=LINE('',#5875,#1300);
#1007=LINE('',#5877,#1301);
#1008=LINE('',#5878,#1302);
#1009=LINE('',#5881,#1303);
#1010=LINE('',#5883,#1304);
#1011=LINE('',#5884,#1305);
#1012=LINE('',#5887,#1306);
#1013=LINE('',#5889,#1307);
#1014=LINE('',#5890,#1308);
#1015=LINE('',#5892,#1309);
#1016=LINE('',#5895,#1310);
#1017=LINE('',#5897,#1311);
#1018=LINE('',#5899,#1312);
#1019=LINE('',#5901,#1313);
#1020=LINE('',#5902,#1314);
#1021=LINE('',#5905,#1315);
#1022=LINE('',#5907,#1316);
#1023=LINE('',#5908,#1317);
#1024=LINE('',#5915,#1318);
#1025=LINE('',#5916,#1319);
#1026=LINE('',#5919,#1320);
#1027=LINE('',#5920,#1321);
#1028=LINE('',#5926,#1322);
#1029=LINE('',#5928,#1323);
#1030=LINE('',#5930,#1324);
#1299=VECTOR('',#4658,10.);
#1300=VECTOR('',#4659,10.);
#1301=VECTOR('',#4660,10.);
#1302=VECTOR('',#4661,10.);
#1303=VECTOR('',#4664,10.);
#1304=VECTOR('',#4665,10.);
#1305=VECTOR('',#4666,10.);
#1306=VECTOR('',#4669,10.);
#1307=VECTOR('',#4670,10.);
#1308=VECTOR('',#4671,10.);
#1309=VECTOR('',#4674,10.);
#1310=VECTOR('',#4677,10.);
#1311=VECTOR('',#4678,10.);
#1312=VECTOR('',#4679,10.);
#1313=VECTOR('',#4680,10.);
#1314=VECTOR('',#4681,10.);
#1315=VECTOR('',#4684,10.);
#1316=VECTOR('',#4685,10.);
#1317=VECTOR('',#4686,10.);
#1318=VECTOR('',#4693,10.);
#1319=VECTOR('',#4694,10.);
#1320=VECTOR('',#4697,10.);
#1321=VECTOR('',#4698,10.);
#1322=VECTOR('',#4705,10.);
#1323=VECTOR('',#4708,3.25);
#1324=VECTOR('',#4711,3.25);
#1657=VERTEX_POINT('',#5871);
#1658=VERTEX_POINT('',#5872);
#1659=VERTEX_POINT('',#5874);
#1660=VERTEX_POINT('',#5876);
#1661=VERTEX_POINT('',#5880);
#1662=VERTEX_POINT('',#5882);
#1663=VERTEX_POINT('',#5886);
#1664=VERTEX_POINT('',#5888);
#1665=VERTEX_POINT('',#5894);
#1666=VERTEX_POINT('',#5896);
#1667=VERTEX_POINT('',#5898);
#1668=VERTEX_POINT('',#5900);
#1669=VERTEX_POINT('',#5904);
#1670=VERTEX_POINT('',#5906);
#1671=VERTEX_POINT('',#5909);
#1672=VERTEX_POINT('',#5911);
#1673=VERTEX_POINT('',#5914);
#1674=VERTEX_POINT('',#5918);
#1675=VERTEX_POINT('',#5921);
#1676=VERTEX_POINT('',#5923);
#2089=EDGE_CURVE('',#1657,#1658,#1005,.T.);
#2090=EDGE_CURVE('',#1659,#1657,#1006,.T.);
#2091=EDGE_CURVE('',#1659,#1660,#1007,.T.);
#2092=EDGE_CURVE('',#1658,#1660,#1008,.T.);
#2093=EDGE_CURVE('',#1658,#1661,#1009,.T.);
#2094=EDGE_CURVE('',#1660,#1662,#1010,.T.);
#2095=EDGE_CURVE('',#1661,#1662,#1011,.T.);
#2096=EDGE_CURVE('',#1661,#1663,#1012,.T.);
#2097=EDGE_CURVE('',#1662,#1664,#1013,.T.);
#2098=EDGE_CURVE('',#1663,#1664,#1014,.T.);
#2099=EDGE_CURVE('',#1664,#1659,#1015,.T.);
#2100=EDGE_CURVE('',#1665,#1663,#1016,.T.);
#2101=EDGE_CURVE('',#1666,#1665,#1017,.T.);
#2102=EDGE_CURVE('',#1667,#1666,#1018,.T.);
#2103=EDGE_CURVE('',#1668,#1667,#1019,.T.);
#2104=EDGE_CURVE('',#1657,#1668,#1020,.T.);
#2105=EDGE_CURVE('',#1666,#1669,#1021,.T.);
#2106=EDGE_CURVE('',#1669,#1670,#1022,.T.);
#2107=EDGE_CURVE('',#1670,#1667,#1023,.T.);
#2108=EDGE_CURVE('',#1671,#1671,#780,.T.);
#2109=EDGE_CURVE('',#1672,#1672,#781,.T.);
#2110=EDGE_CURVE('',#1673,#1670,#1024,.T.);
#2111=EDGE_CURVE('',#1668,#1673,#1025,.T.);
#2112=EDGE_CURVE('',#1673,#1674,#1026,.T.);
#2113=EDGE_CURVE('',#1674,#1665,#1027,.T.);
#2114=EDGE_CURVE('',#1675,#1675,#782,.F.);
#2115=EDGE_CURVE('',#1676,#1676,#783,.F.);
#2116=EDGE_CURVE('',#1674,#1669,#1028,.T.);
#2117=EDGE_CURVE('',#1672,#1676,#1029,.T.);
#2118=EDGE_CURVE('',#1671,#1675,#1030,.T.);
#2909=ORIENTED_EDGE('',*,*,#2089,.F.);
#2910=ORIENTED_EDGE('',*,*,#2090,.F.);
#2911=ORIENTED_EDGE('',*,*,#2091,.T.);
#2912=ORIENTED_EDGE('',*,*,#2092,.F.);
#2913=ORIENTED_EDGE('',*,*,#2093,.F.);
#2914=ORIENTED_EDGE('',*,*,#2092,.T.);
#2915=ORIENTED_EDGE('',*,*,#2094,.T.);
#2916=ORIENTED_EDGE('',*,*,#2095,.F.);
#2917=ORIENTED_EDGE('',*,*,#2096,.F.);
#2918=ORIENTED_EDGE('',*,*,#2095,.T.);
#2919=ORIENTED_EDGE('',*,*,#2097,.T.);
#2920=ORIENTED_EDGE('',*,*,#2098,.F.);
#2921=ORIENTED_EDGE('',*,*,#2099,.F.);
#2922=ORIENTED_EDGE('',*,*,#2097,.F.);
#2923=ORIENTED_EDGE('',*,*,#2094,.F.);
#2924=ORIENTED_EDGE('',*,*,#2091,.F.);
#2925=ORIENTED_EDGE('',*,*,#2089,.T.);
#2926=ORIENTED_EDGE('',*,*,#2093,.T.);
#2927=ORIENTED_EDGE('',*,*,#2096,.T.);
#2928=ORIENTED_EDGE('',*,*,#2100,.F.);
#2929=ORIENTED_EDGE('',*,*,#2101,.F.);
#2930=ORIENTED_EDGE('',*,*,#2102,.F.);
#2931=ORIENTED_EDGE('',*,*,#2103,.F.);
#2932=ORIENTED_EDGE('',*,*,#2104,.F.);
#2933=ORIENTED_EDGE('',*,*,#2102,.T.);
#2934=ORIENTED_EDGE('',*,*,#2105,.T.);
#2935=ORIENTED_EDGE('',*,*,#2106,.T.);
#2936=ORIENTED_EDGE('',*,*,#2107,.T.);
#2937=ORIENTED_EDGE('',*,*,#2108,.T.);
#2938=ORIENTED_EDGE('',*,*,#2109,.T.);
#2939=ORIENTED_EDGE('',*,*,#2103,.T.);
#2940=ORIENTED_EDGE('',*,*,#2107,.F.);
#2941=ORIENTED_EDGE('',*,*,#2110,.F.);
#2942=ORIENTED_EDGE('',*,*,#2111,.F.);
#2943=ORIENTED_EDGE('',*,*,#2090,.T.);
#2944=ORIENTED_EDGE('',*,*,#2104,.T.);
#2945=ORIENTED_EDGE('',*,*,#2111,.T.);
#2946=ORIENTED_EDGE('',*,*,#2112,.T.);
#2947=ORIENTED_EDGE('',*,*,#2113,.T.);
#2948=ORIENTED_EDGE('',*,*,#2100,.T.);
#2949=ORIENTED_EDGE('',*,*,#2098,.T.);
#2950=ORIENTED_EDGE('',*,*,#2099,.T.);
#2951=ORIENTED_EDGE('',*,*,#2114,.T.);
#2952=ORIENTED_EDGE('',*,*,#2115,.T.);
#2953=ORIENTED_EDGE('',*,*,#2101,.T.);
#2954=ORIENTED_EDGE('',*,*,#2113,.F.);
#2955=ORIENTED_EDGE('',*,*,#2116,.T.);
#2956=ORIENTED_EDGE('',*,*,#2105,.F.);
#2957=ORIENTED_EDGE('',*,*,#2109,.F.);
#2958=ORIENTED_EDGE('',*,*,#2117,.T.);
#2959=ORIENTED_EDGE('',*,*,#2115,.F.);
#2960=ORIENTED_EDGE('',*,*,#2117,.F.);
#2961=ORIENTED_EDGE('',*,*,#2108,.F.);
#2962=ORIENTED_EDGE('',*,*,#2118,.T.);
#2963=ORIENTED_EDGE('',*,*,#2114,.F.);
#2964=ORIENTED_EDGE('',*,*,#2118,.F.);
#2965=ORIENTED_EDGE('',*,*,#2112,.F.);
#2966=ORIENTED_EDGE('',*,*,#2110,.T.);
#2967=ORIENTED_EDGE('',*,*,#2106,.F.);
#2968=ORIENTED_EDGE('',*,*,#2116,.F.);
#3202=CYLINDRICAL_SURFACE('',#3824,2.5175);
#3203=CYLINDRICAL_SURFACE('',#3825,2.5175);
#3343=ADVANCED_FACE('',(#401),#219,.F.);
#3344=ADVANCED_FACE('',(#402),#220,.F.);
#3345=ADVANCED_FACE('',(#403),#221,.F.);
#3346=ADVANCED_FACE('',(#404),#222,.F.);
#3347=ADVANCED_FACE('',(#405),#223,.F.);
#3348=ADVANCED_FACE('',(#406,#117,#118),#224,.T.);
#3349=ADVANCED_FACE('',(#407),#225,.T.);
#3350=ADVANCED_FACE('',(#408,#119,#120),#226,.F.);
#3351=ADVANCED_FACE('',(#409),#227,.T.);
#3352=ADVANCED_FACE('',(#410),#3202,.F.);
#3353=ADVANCED_FACE('',(#411),#3203,.F.);
#3354=ADVANCED_FACE('',(#412),#228,.T.);
#3403=CLOSED_SHELL('',(#3343,#3344,#3345,#3346,#3347,#3348,#3349,#3350,
#3351,#3352,#3353,#3354));
#3810=AXIS2_PLACEMENT_3D('',#5869,#4654,#4655);
#3811=AXIS2_PLACEMENT_3D('',#5870,#4656,#4657);
#3812=AXIS2_PLACEMENT_3D('',#5879,#4662,#4663);
#3813=AXIS2_PLACEMENT_3D('',#5885,#4667,#4668);
#3814=AXIS2_PLACEMENT_3D('',#5891,#4672,#4673);
#3815=AXIS2_PLACEMENT_3D('',#5893,#4675,#4676);
#3816=AXIS2_PLACEMENT_3D('',#5903,#4682,#4683);
#3817=AXIS2_PLACEMENT_3D('',#5910,#4687,#4688);
#3818=AXIS2_PLACEMENT_3D('',#5912,#4689,#4690);
#3819=AXIS2_PLACEMENT_3D('',#5913,#4691,#4692);
#3820=AXIS2_PLACEMENT_3D('',#5917,#4695,#4696);
#3821=AXIS2_PLACEMENT_3D('',#5922,#4699,#4700);
#3822=AXIS2_PLACEMENT_3D('',#5924,#4701,#4702);
#3823=AXIS2_PLACEMENT_3D('',#5925,#4703,#4704);
#3824=AXIS2_PLACEMENT_3D('',#5927,#4706,#4707);
#3825=AXIS2_PLACEMENT_3D('',#5929,#4709,#4710);
#3826=AXIS2_PLACEMENT_3D('',#5931,#4712,#4713);
#4654=DIRECTION('axis',(0.,0.,1.));
#4655=DIRECTION('refdir',(1.,0.,0.));
#4656=DIRECTION('center_axis',(0.,-1.,0.));
#4657=DIRECTION('ref_axis',(0.,0.,1.));
#4658=DIRECTION('',(0.,0.,1.));
#4659=DIRECTION('',(1.,0.,0.));
#4660=DIRECTION('',(0.,0.,1.));
#4661=DIRECTION('',(-1.,0.,0.));
#4662=DIRECTION('center_axis',(0.,0.,1.));
#4663=DIRECTION('ref_axis',(0.,1.,0.));
#4664=DIRECTION('',(0.,1.,0.));
#4665=DIRECTION('',(0.,1.,0.));
#4666=DIRECTION('',(-1.,0.,0.));
#4667=DIRECTION('center_axis',(0.,1.,0.));
#4668=DIRECTION('ref_axis',(0.,0.,-1.));
#4669=DIRECTION('',(0.,0.,-1.));
#4670=DIRECTION('',(0.,0.,-1.));
#4671=DIRECTION('',(-1.,0.,0.));
#4672=DIRECTION('center_axis',(-1.,0.,0.));
#4673=DIRECTION('ref_axis',(0.,0.,1.));
#4674=DIRECTION('',(0.,-1.,0.));
#4675=DIRECTION('center_axis',(-1.,0.,0.));
#4676=DIRECTION('ref_axis',(0.,1.,0.));
#4677=DIRECTION('',(0.,-1.,0.));
#4678=DIRECTION('',(0.,0.,-1.));
#4679=DIRECTION('',(0.,1.,0.));
#4680=DIRECTION('',(0.,0.,1.));
#4681=DIRECTION('',(0.,-1.,0.));
#4682=DIRECTION('center_axis',(0.,0.,1.));
#4683=DIRECTION('ref_axis',(1.,0.,0.));
#4684=DIRECTION('',(-1.,0.,0.));
#4685=DIRECTION('',(0.,-1.,0.));
#4686=DIRECTION('',(1.,0.,0.));
#4687=DIRECTION('center_axis',(0.,0.,-1.));
#4688=DIRECTION('ref_axis',(1.,0.,0.));
#4689=DIRECTION('center_axis',(0.,0.,-1.));
#4690=DIRECTION('ref_axis',(1.,0.,0.));
#4691=DIRECTION('center_axis',(0.,-1.,0.));
#4692=DIRECTION('ref_axis',(1.,0.,0.));
#4693=DIRECTION('',(0.,0.,1.));
#4694=DIRECTION('',(-1.,0.,0.));
#4695=DIRECTION('center_axis',(0.,0.,1.));
#4696=DIRECTION('ref_axis',(1.,0.,0.));
#4697=DIRECTION('',(0.,1.,0.));
#4698=DIRECTION('',(1.,0.,0.));
#4699=DIRECTION('center_axis',(0.,0.,-1.));
#4700=DIRECTION('ref_axis',(1.,0.,0.));
#4701=DIRECTION('center_axis',(0.,0.,-1.));
#4702=DIRECTION('ref_axis',(1.,0.,0.));
#4703=DIRECTION('center_axis',(0.,1.,0.));
#4704=DIRECTION('ref_axis',(-1.,0.,0.));
#4705=DIRECTION('',(0.,0.,1.));
#4706=DIRECTION('center_axis',(0.,0.,-1.));
#4707=DIRECTION('ref_axis',(1.,0.,0.));
#4708=DIRECTION('',(0.,0.,-1.));
#4709=DIRECTION('center_axis',(0.,0.,1.));
#4710=DIRECTION('ref_axis',(1.,0.,0.));
#4711=DIRECTION('',(0.,0.,-1.));
#4712=DIRECTION('center_axis',(-1.,0.,0.));
#4713=DIRECTION('ref_axis',(0.,-1.,0.));
#5869=CARTESIAN_POINT('',(0.,0.,0.));
#5870=CARTESIAN_POINT('Origin',(-29.1374542444053,-4.,0.));
#5871=CARTESIAN_POINT('',(-29.6374542444053,-4.,0.));
#5872=CARTESIAN_POINT('',(-29.6374542444053,-4.,6.));
#5873=CARTESIAN_POINT('',(-29.6374542444053,-4.,8.));
#5874=CARTESIAN_POINT('',(-35.1374542444053,-4.,0.));
#5875=CARTESIAN_POINT('',(-14.5687271222026,-4.,0.));
#5876=CARTESIAN_POINT('',(-35.1374542444053,-4.,6.));
#5877=CARTESIAN_POINT('',(-35.1374542444053,-4.,-6.));
#5878=CARTESIAN_POINT('',(-29.1374542444053,-4.,6.));
#5879=CARTESIAN_POINT('Origin',(-29.1374542444053,-4.,6.));
#5880=CARTESIAN_POINT('',(-29.6374542444053,4.,6.));
#5881=CARTESIAN_POINT('',(-29.6374542444053,-17.,6.));
#5882=CARTESIAN_POINT('',(-35.1374542444053,4.,6.));
#5883=CARTESIAN_POINT('',(-35.1374542444053,-4.,6.));
#5884=CARTESIAN_POINT('',(-29.1374542444053,4.,6.));
#5885=CARTESIAN_POINT('Origin',(-29.1374542444053,4.,6.));
#5886=CARTESIAN_POINT('',(-29.6374542444053,4.,0.));
#5887=CARTESIAN_POINT('',(-29.6374542444053,4.,11.));
#5888=CARTESIAN_POINT('',(-35.1374542444053,4.,0.));
#5889=CARTESIAN_POINT('',(-35.1374542444053,4.,6.));
#5890=CARTESIAN_POINT('',(-14.5687271222026,4.,0.));
#5891=CARTESIAN_POINT('Origin',(-35.1374542444053,0.,3.));
#5892=CARTESIAN_POINT('',(-35.1374542444053,0.,0.));
#5893=CARTESIAN_POINT('Origin',(-29.6374542444053,-30.,16.));
#5894=CARTESIAN_POINT('',(-29.6374542444053,30.,0.));
#5895=CARTESIAN_POINT('',(-29.6374542444053,-15.,0.));
#5896=CARTESIAN_POINT('',(-29.6374542444053,30.,16.));
#5897=CARTESIAN_POINT('',(-29.6374542444053,30.,8.));
#5898=CARTESIAN_POINT('',(-29.6374542444053,-30.,16.));
#5899=CARTESIAN_POINT('',(-29.6374542444053,-15.,16.));
#5900=CARTESIAN_POINT('',(-29.6374542444053,-30.,0.));
#5901=CARTESIAN_POINT('',(-29.6374542444053,-30.,8.));
#5902=CARTESIAN_POINT('',(-29.6374542444053,-15.,0.));
#5903=CARTESIAN_POINT('Origin',(0.,0.,16.));
#5904=CARTESIAN_POINT('',(-50.,30.,16.));
#5905=CARTESIAN_POINT('',(-50.,30.,16.));
#5906=CARTESIAN_POINT('',(-50.,-30.,16.));
#5907=CARTESIAN_POINT('',(-50.,-30.,16.));
#5908=CARTESIAN_POINT('',(50.,-30.,16.));
#5909=CARTESIAN_POINT('',(-44.5175,-22.,16.));
#5910=CARTESIAN_POINT('Origin',(-42.,-22.,16.));
#5911=CARTESIAN_POINT('',(-44.5175,22.,16.));
#5912=CARTESIAN_POINT('Origin',(-42.,22.,16.));
#5913=CARTESIAN_POINT('Origin',(-50.,-30.,0.));
#5914=CARTESIAN_POINT('',(-50.,-30.,0.));
#5915=CARTESIAN_POINT('',(-50.,-30.,0.));
#5916=CARTESIAN_POINT('',(50.,-30.,0.));
#5917=CARTESIAN_POINT('Origin',(0.,0.,0.));
#5918=CARTESIAN_POINT('',(-50.,30.,0.));
#5919=CARTESIAN_POINT('',(-50.,-30.,0.));
#5920=CARTESIAN_POINT('',(-50.,30.,0.));
#5921=CARTESIAN_POINT('',(-44.5175,-22.,0.));
#5922=CARTESIAN_POINT('Origin',(-42.,-22.,0.));
#5923=CARTESIAN_POINT('',(-44.5175,22.,0.));
#5924=CARTESIAN_POINT('Origin',(-42.,22.,0.));
#5925=CARTESIAN_POINT('Origin',(50.,30.,0.));
#5926=CARTESIAN_POINT('',(-50.,30.,0.));
#5927=CARTESIAN_POINT('Origin',(-42.,22.,16.));
#5928=CARTESIAN_POINT('',(-44.5175,22.,16.));
#5929=CARTESIAN_POINT('Origin',(-42.,-22.,16.));
#5930=CARTESIAN_POINT('',(-44.5175,-22.,16.));
#5931=CARTESIAN_POINT('Origin',(-50.,30.,0.));
#7031=UNCERTAINTY_MEASURE_WITH_UNIT(LENGTH_MEASURE(0.01),#7048,
'DISTANCE_ACCURACY_VALUE',
'Maximum model space distance between geometric entities at asserted c
onnectivities');
#7035=UNCERTAINTY_MEASURE_WITH_UNIT(LENGTH_MEASURE(0.01),#7048,
'DISTANCE_ACCURACY_VALUE',
'Maximum model space distance between geometric entities at asserted c
onnectivities');
#7043=(
GEOMETRIC_REPRESENTATION_CONTEXT(3)
GLOBAL_UNCERTAINTY_ASSIGNED_CONTEXT((#7031))
GLOBAL_UNIT_ASSIGNED_CONTEXT((#7048,#7050,#7051))
REPRESENTATION_CONTEXT('','3D')
);
#7047=(
GEOMETRIC_REPRESENTATION_CONTEXT(3)
GLOBAL_UNCERTAINTY_ASSIGNED_CONTEXT((#7035))
GLOBAL_UNIT_ASSIGNED_CONTEXT((#7048,#7050,#7051))
REPRESENTATION_CONTEXT('','3D')
);
#7048=(
LENGTH_UNIT()
NAMED_UNIT(*)
SI_UNIT(.MILLI.,.METRE.)
);
#7050=(
NAMED_UNIT(*)
PLANE_ANGLE_UNIT()
SI_UNIT($,.RADIAN.)
);
#7051=(
NAMED_UNIT(*)
SI_UNIT($,.STERADIAN.)
SOLID_ANGLE_UNIT()
);
#7059=SHAPE_DEFINITION_REPRESENTATION(#7070,#7091);
#7070=PRODUCT_DEFINITION_SHAPE('',$,#7103);
#7091=SHAPE_REPRESENTATION('',(#3810),#7043);
#7095=PRODUCT_DEFINITION_CONTEXT('part definition',#7130,'design');
#7103=PRODUCT_DEFINITION('End_Block','End_Block',#7114,#7095);
#7114=PRODUCT_DEFINITION_FORMATION('',$,#7139);
#7130=APPLICATION_CONTEXT(
'Core Data for Automotive Mechanical Design Process');
#7131=PRODUCT_CONTEXT('part definition',#7130,'mechanical');
#7139=PRODUCT('End_Block','End_Block',$,(#7131));
#7171=COLOUR_RGB('Dark Blue',0.08,0.2,0.34);
#7172=FILL_AREA_STYLE_COLOUR('',#7171);
#7173=FILL_AREA_STYLE('',(#7172));
#7174=SURFACE_STYLE_FILL_AREA(#7173);
#7175=SURFACE_SIDE_STYLE('',(#7174));
#7176=SURFACE_STYLE_USAGE(.BOTH.,#7175);
#7177=PRESENTATION_STYLE_ASSIGNMENT((#7176));
ENDSEC;
END-ISO-10303-21;
